ISO-10303-21;
HEADER;
FILE_DESCRIPTION((''),'2;1');
FILE_NAME('LINCH_PIN.step','2026-10-01T22:06:14-07:00',(''),(''),'','','');
FILE_SCHEMA (('AUTOMOTIVE_DESIGN { 1 0 10303 214 3 1 1 }'));
ENDSEC;
DATA;
#10=MECHANICAL_DESIGN_GEOMETRIC_PRESENTATION_REPRESENTATION('',(#1036),#50440);
#46=B_SPLINE_CURVE_WITH_KNOTS('',3,(#50119,#50120,#50121,#50122,#50123,
#50124,#50125,#50126,#50127,#50128,#50129,#50130,#50131,#50132,#50133,#50134,
#50135,#50136,#50137,#50138,#50139,#50140),.UNSPECIFIED.,.F.,.F.,(4,2,2,
2,2,2,2,2,2,2,4),(0.921102242512175,0.924013514464762,0.972179762855851,
1.06851225963803,1.16823933679329,1.26796641394856,1.36769349110382,1.46742056825909,
1.56375306504127,1.61191931343235,1.61483058538494),.UNSPECIFIED.) ;
#47=B_SPLINE_CURVE_WITH_KNOTS('',3,(#50266,#50267,#50268,#50269,#50270,
#50271,#50272,#50273,#50274,#50275,#50276,#50277),.UNSPECIFIED.,.F.,.F.,
(4,2,2,2,2,4),(0.0455189062767866,0.0517682265718383,0.103536453143677,
0.207072906287353,0.299969895185651,0.392866884083948),.UNSPECIFIED.) ;
#48=B_SPLINE_CURVE_WITH_KNOTS('',3,(#50281,#50282,#50283,#50284,#50285,
#50286,#50287,#50288,#50289,#50290,#50291,#50292),.UNSPECIFIED.,.F.,.F.,
(4,2,2,2,2,4),(0.392866884083948,0.485763872982246,0.578660861880544,0.68219731502422,
0.733965541596058,0.74021486189111),.UNSPECIFIED.) ;
#676=ELLIPSE('',#32279,0.965925826289068,0.25) ;
#677=ELLIPSE('',#32280,0.965925826289068,0.25) ;
#678=ELLIPSE('',#32281,0.258819045102521,0.25) ;
#679=ELLIPSE('',#32282,0.258819045102521,0.25) ;
#680=ELLIPSE('',#32284,0.258819045102521,0.25) ;
#681=ELLIPSE('',#32285,0.258819045102521,0.25) ;
#682=ELLIPSE('',#32331,0.258819045102521,0.25) ;
#683=ELLIPSE('',#32332,0.258819045102521,0.25) ;
#684=ELLIPSE('',#32333,0.258819045102521,0.25) ;
#685=ELLIPSE('',#32334,0.258819045102521,0.25) ;
#686=ELLIPSE('',#32336,0.258819045102521,0.25) ;
#687=ELLIPSE('',#32337,0.258819045102521,0.25) ;
#688=ELLIPSE('',#32339,0.258819045102521,0.25) ;
#689=ELLIPSE('',#32340,0.258819045102521,0.25) ;
#690=ELLIPSE('',#32342,0.258819045102521,0.25) ;
#691=ELLIPSE('',#32344,0.258819045102521,0.25) ;
#692=ELLIPSE('',#32346,0.258819045102521,0.25) ;
#693=ELLIPSE('',#32348,0.258819045102521,0.25) ;
#694=ELLIPSE('',#32350,0.258819045102521,0.25) ;
#695=ELLIPSE('',#32352,0.965925826289069,0.25) ;
#696=ELLIPSE('',#32353,0.965925826289069,0.25) ;
#697=ELLIPSE('',#32355,0.258819045102521,0.25) ;
#698=ELLIPSE('',#32356,0.258819045102521,0.25) ;
#880=SPHERICAL_SURFACE('',#32286,0.25) ;
#881=SPHERICAL_SURFACE('',#32289,0.25) ;
#882=SPHERICAL_SURFACE('',#32292,0.25) ;
#883=SPHERICAL_SURFACE('',#32295,0.25) ;
#884=SPHERICAL_SURFACE('',#32300,0.25) ;
#885=SPHERICAL_SURFACE('',#32305,0.25) ;
#886=SPHERICAL_SURFACE('',#32310,0.25) ;
#887=SPHERICAL_SURFACE('',#32315,0.25) ;
#888=SPHERICAL_SURFACE('',#32320,0.25) ;
#889=SPHERICAL_SURFACE('',#32325,0.25) ;
#890=SPHERICAL_SURFACE('',#32327,0.25) ;
#935=SHAPE_REPRESENTATION_RELATIONSHIP('SRR','None',#50670,#980) ;
#980=ADVANCED_BREP_SHAPE_REPRESENTATION('',(#1089),#50439) ;
#1036=STYLED_ITEM('',(#50883),#1089) ;
#1089=MANIFOLD_SOLID_BREP('LINCH_PIN',#28714) ;
#2337=PLANE('',#32358) ;
#2338=PLANE('',#32363) ;
#2339=PLANE('',#32364) ;
#3867=FACE_OUTER_BOUND('',#5717,.T.) ;
#3868=FACE_OUTER_BOUND('',#5718,.T.) ;
#3869=FACE_OUTER_BOUND('',#5719,.T.) ;
#3870=FACE_OUTER_BOUND('',#5720,.T.) ;
#3871=FACE_OUTER_BOUND('',#5721,.T.) ;
#3872=FACE_OUTER_BOUND('',#5722,.T.) ;
#3873=FACE_OUTER_BOUND('',#5723,.T.) ;
#3874=FACE_OUTER_BOUND('',#5724,.T.) ;
#3875=FACE_OUTER_BOUND('',#5725,.T.) ;
#3876=FACE_OUTER_BOUND('',#5726,.T.) ;
#3877=FACE_OUTER_BOUND('',#5727,.T.) ;
#3878=FACE_OUTER_BOUND('',#5728,.T.) ;
#3879=FACE_OUTER_BOUND('',#5729,.T.) ;
#3880=FACE_OUTER_BOUND('',#5730,.T.) ;
#3881=FACE_OUTER_BOUND('',#5731,.T.) ;
#3882=FACE_OUTER_BOUND('',#5732,.T.) ;
#3883=FACE_OUTER_BOUND('',#5733,.T.) ;
#3884=FACE_OUTER_BOUND('',#5734,.T.) ;
#3885=FACE_OUTER_BOUND('',#5735,.T.) ;
#3886=FACE_OUTER_BOUND('',#5736,.T.) ;
#3887=FACE_OUTER_BOUND('',#5737,.T.) ;
#3888=FACE_OUTER_BOUND('',#5738,.T.) ;
#3889=FACE_OUTER_BOUND('',#5739,.T.) ;
#3890=FACE_OUTER_BOUND('',#5740,.T.) ;
#3891=FACE_OUTER_BOUND('',#5741,.T.) ;
#3892=FACE_OUTER_BOUND('',#5742,.T.) ;
#3893=FACE_OUTER_BOUND('',#5743,.T.) ;
#5717=EDGE_LOOP('',(#26499,#26500,#26501,#26502,#26503,#26504,#26505,#26506,
#26507,#26508)) ;
#5718=EDGE_LOOP('',(#26509,#26510)) ;
#5719=EDGE_LOOP('',(#26511,#26512)) ;
#5720=EDGE_LOOP('',(#26513,#26514)) ;
#5721=EDGE_LOOP('',(#26515,#26516,#26517,#26518,#26519)) ;
#5722=EDGE_LOOP('',(#26520,#26521,#26522,#26523)) ;
#5723=EDGE_LOOP('',(#26524,#26525,#26526,#26527)) ;
#5724=EDGE_LOOP('',(#26528,#26529,#26530,#26531)) ;
#5725=EDGE_LOOP('',(#26532,#26533,#26534,#26535)) ;
#5726=EDGE_LOOP('',(#26536,#26537,#26538,#26539)) ;
#5727=EDGE_LOOP('',(#26540,#26541)) ;
#5728=EDGE_LOOP('',(#26542,#26543)) ;
#5729=EDGE_LOOP('',(#26544,#26545,#26546,#26547,#26548,#26549,#26550,#26551)) ;
#5730=EDGE_LOOP('',(#26552,#26553,#26554,#26555,#26556,#26557,#26558,#26559)) ;
#5731=EDGE_LOOP('',(#26560,#26561,#26562,#26563,#26564,#26565,#26566,#26567)) ;
#5732=EDGE_LOOP('',(#26568,#26569,#26570,#26571,#26572,#26573,#26574,#26575,
#26576)) ;
#5733=EDGE_LOOP('',(#26577,#26578,#26579,#26580,#26581,#26582,#26583,#26584)) ;
#5734=EDGE_LOOP('',(#26585,#26586,#26587,#26588,#26589,#26590,#26591,#26592)) ;
#5735=EDGE_LOOP('',(#26593,#26594,#26595,#26596,#26597,#26598,#26599,#26600)) ;
#5736=EDGE_LOOP('',(#26601,#26602,#26603,#26604,#26605,#26606,#26607,#26608)) ;
#5737=EDGE_LOOP('',(#26609,#26610,#26611,#26612,#26613,#26614,#26615,#26616,
#26617,#26618,#26619)) ;
#5738=EDGE_LOOP('',(#26620,#26621,#26622,#26623,#26624,#26625,#26626,#26627)) ;
#5739=EDGE_LOOP('',(#26628,#26629,#26630,#26631,#26632,#26633,#26634,#26635)) ;
#5740=EDGE_LOOP('',(#26636,#26637,#26638)) ;
#5741=EDGE_LOOP('',(#26639,#26640,#26641,#26642,#26643,#26644,#26645,#26646)) ;
#5742=EDGE_LOOP('',(#26647)) ;
#5743=EDGE_LOOP('',(#26648,#26649,#26650)) ;
#8203=LINE('',#50146,#10675) ;
#8204=LINE('',#50234,#10676) ;
#8205=LINE('',#50239,#10677) ;
#8206=LINE('',#50244,#10678) ;
#8207=LINE('',#50248,#10679) ;
#8208=LINE('',#50251,#10680) ;
#8209=LINE('',#50254,#10681) ;
#8210=LINE('',#50257,#10682) ;
#8211=LINE('',#50260,#10683) ;
#8212=LINE('',#50264,#10684) ;
#8213=LINE('',#50295,#10685) ;
#8214=LINE('',#50299,#10686) ;
#8215=LINE('',#50304,#10687) ;
#10675=VECTOR('',#40992,0.25) ;
#10676=VECTOR('',#41095,0.25) ;
#10677=VECTOR('',#41102,0.25) ;
#10678=VECTOR('',#41109,0.25) ;
#10679=VECTOR('',#41116,0.25) ;
#10680=VECTOR('',#41121,0.25) ;
#10681=VECTOR('',#41126,0.25) ;
#10682=VECTOR('',#41131,0.25) ;
#10683=VECTOR('',#41136,0.25) ;
#10684=VECTOR('',#41141,0.25) ;
#10685=VECTOR('',#41148,0.25) ;
#10686=VECTOR('',#41155,0.25) ;
#10687=VECTOR('',#41162,0.3) ;
#11818=CIRCLE('',#32283,0.25) ;
#11819=CIRCLE('',#32287,0.25) ;
#11820=CIRCLE('',#32288,0.25) ;
#11821=CIRCLE('',#32290,0.25) ;
#11822=CIRCLE('',#32291,0.25) ;
#11823=CIRCLE('',#32293,0.25) ;
#11824=CIRCLE('',#32294,0.25) ;
#11825=CIRCLE('',#32296,0.25) ;
#11826=CIRCLE('',#32297,0.25) ;
#11827=CIRCLE('',#32298,0.25) ;
#11828=CIRCLE('',#32299,0.25) ;
#11829=CIRCLE('',#32301,0.25) ;
#11830=CIRCLE('',#32302,0.25) ;
#11831=CIRCLE('',#32303,0.25) ;
#11832=CIRCLE('',#32304,0.25) ;
#11833=CIRCLE('',#32306,0.25) ;
#11834=CIRCLE('',#32307,0.25) ;
#11835=CIRCLE('',#32308,0.25) ;
#11836=CIRCLE('',#32309,0.25) ;
#11837=CIRCLE('',#32311,0.25) ;
#11838=CIRCLE('',#32312,0.25) ;
#11839=CIRCLE('',#32313,0.25) ;
#11840=CIRCLE('',#32314,0.25) ;
#11841=CIRCLE('',#32316,0.25) ;
#11842=CIRCLE('',#32317,0.25) ;
#11843=CIRCLE('',#32318,0.25) ;
#11844=CIRCLE('',#32319,0.25) ;
#11845=CIRCLE('',#32321,0.25) ;
#11846=CIRCLE('',#32322,0.25) ;
#11847=CIRCLE('',#32323,0.25) ;
#11848=CIRCLE('',#32324,0.25) ;
#11849=CIRCLE('',#32326,0.25) ;
#11850=CIRCLE('',#32328,0.25) ;
#11851=CIRCLE('',#32329,0.25) ;
#11852=CIRCLE('',#32359,0.3) ;
#11853=CIRCLE('',#32361,0.3) ;
#11854=CIRCLE('',#32362,0.3) ;
#14512=VERTEX_POINT('',#50115) ;
#14513=VERTEX_POINT('',#50116) ;
#14514=VERTEX_POINT('',#50118) ;
#14515=VERTEX_POINT('',#50141) ;
#14516=VERTEX_POINT('',#50143) ;
#14517=VERTEX_POINT('',#50145) ;
#14518=VERTEX_POINT('',#50147) ;
#14519=VERTEX_POINT('',#50149) ;
#14520=VERTEX_POINT('',#50154) ;
#14521=VERTEX_POINT('',#50155) ;
#14522=VERTEX_POINT('',#50159) ;
#14523=VERTEX_POINT('',#50160) ;
#14524=VERTEX_POINT('',#50164) ;
#14525=VERTEX_POINT('',#50165) ;
#14526=VERTEX_POINT('',#50169) ;
#14527=VERTEX_POINT('',#50170) ;
#14528=VERTEX_POINT('',#50172) ;
#14529=VERTEX_POINT('',#50174) ;
#14530=VERTEX_POINT('',#50178) ;
#14531=VERTEX_POINT('',#50179) ;
#14532=VERTEX_POINT('',#50181) ;
#14533=VERTEX_POINT('',#50183) ;
#14534=VERTEX_POINT('',#50187) ;
#14535=VERTEX_POINT('',#50188) ;
#14536=VERTEX_POINT('',#50190) ;
#14537=VERTEX_POINT('',#50192) ;
#14538=VERTEX_POINT('',#50196) ;
#14539=VERTEX_POINT('',#50197) ;
#14540=VERTEX_POINT('',#50199) ;
#14541=VERTEX_POINT('',#50201) ;
#14542=VERTEX_POINT('',#50205) ;
#14543=VERTEX_POINT('',#50206) ;
#14544=VERTEX_POINT('',#50208) ;
#14545=VERTEX_POINT('',#50210) ;
#14546=VERTEX_POINT('',#50214) ;
#14547=VERTEX_POINT('',#50215) ;
#14548=VERTEX_POINT('',#50217) ;
#14549=VERTEX_POINT('',#50219) ;
#14550=VERTEX_POINT('',#50225) ;
#14551=VERTEX_POINT('',#50226) ;
#14552=VERTEX_POINT('',#50230) ;
#14553=VERTEX_POINT('',#50233) ;
#14554=VERTEX_POINT('',#50238) ;
#14555=VERTEX_POINT('',#50243) ;
#14556=VERTEX_POINT('',#50263) ;
#14557=VERTEX_POINT('',#50265) ;
#14558=VERTEX_POINT('',#50279) ;
#14559=VERTEX_POINT('',#50294) ;
#14560=VERTEX_POINT('',#50303) ;
#18515=EDGE_CURVE('',#14512,#14513,#676,.T.) ;
#18516=EDGE_CURVE('',#14514,#14512,#46,.T.) ;
#18517=EDGE_CURVE('',#14515,#14514,#677,.T.) ;
#18518=EDGE_CURVE('',#14515,#14516,#678,.T.) ;
#18519=EDGE_CURVE('',#14516,#14517,#8203,.T.) ;
#18520=EDGE_CURVE('',#14518,#14517,#679,.T.) ;
#18521=EDGE_CURVE('',#14519,#14518,#11818,.T.) ;
#18522=EDGE_CURVE('',#14517,#14519,#680,.T.) ;
#18523=EDGE_CURVE('',#14516,#14513,#681,.T.) ;
#18524=EDGE_CURVE('',#14520,#14521,#11819,.T.) ;
#18525=EDGE_CURVE('',#14521,#14520,#11820,.T.) ;
#18526=EDGE_CURVE('',#14522,#14523,#11821,.T.) ;
#18527=EDGE_CURVE('',#14523,#14522,#11822,.T.) ;
#18528=EDGE_CURVE('',#14524,#14525,#11823,.T.) ;
#18529=EDGE_CURVE('',#14525,#14524,#11824,.T.) ;
#18530=EDGE_CURVE('',#14526,#14527,#11825,.T.) ;
#18531=EDGE_CURVE('',#14527,#14528,#11826,.T.) ;
#18532=EDGE_CURVE('',#14529,#14528,#11827,.T.) ;
#18533=EDGE_CURVE('',#14528,#14526,#11828,.T.) ;
#18534=EDGE_CURVE('',#14530,#14531,#11829,.T.) ;
#18535=EDGE_CURVE('',#14531,#14532,#11830,.T.) ;
#18536=EDGE_CURVE('',#14532,#14533,#11831,.T.) ;
#18537=EDGE_CURVE('',#14533,#14530,#11832,.T.) ;
#18538=EDGE_CURVE('',#14534,#14535,#11833,.T.) ;
#18539=EDGE_CURVE('',#14535,#14536,#11834,.T.) ;
#18540=EDGE_CURVE('',#14536,#14537,#11835,.T.) ;
#18541=EDGE_CURVE('',#14537,#14534,#11836,.T.) ;
#18542=EDGE_CURVE('',#14538,#14539,#11837,.T.) ;
#18543=EDGE_CURVE('',#14539,#14540,#11838,.T.) ;
#18544=EDGE_CURVE('',#14540,#14541,#11839,.T.) ;
#18545=EDGE_CURVE('',#14541,#14538,#11840,.T.) ;
#18546=EDGE_CURVE('',#14542,#14543,#11841,.T.) ;
#18547=EDGE_CURVE('',#14543,#14544,#11842,.T.) ;
#18548=EDGE_CURVE('',#14544,#14545,#11843,.T.) ;
#18549=EDGE_CURVE('',#14545,#14542,#11844,.T.) ;
#18550=EDGE_CURVE('',#14546,#14547,#11845,.T.) ;
#18551=EDGE_CURVE('',#14547,#14548,#11846,.T.) ;
#18552=EDGE_CURVE('',#14548,#14549,#11847,.T.) ;
#18553=EDGE_CURVE('',#14549,#14546,#11848,.T.) ;
#18554=EDGE_CURVE('',#14518,#14519,#11849,.T.) ;
#18555=EDGE_CURVE('',#14550,#14551,#11850,.T.) ;
#18556=EDGE_CURVE('',#14551,#14550,#11851,.T.) ;
#18557=EDGE_CURVE('',#14521,#14552,#682,.T.) ;
#18558=EDGE_CURVE('',#14552,#14520,#683,.T.) ;
#18559=EDGE_CURVE('',#14552,#14553,#8204,.T.) ;
#18560=EDGE_CURVE('',#14523,#14553,#684,.T.) ;
#18561=EDGE_CURVE('',#14553,#14522,#685,.T.) ;
#18562=EDGE_CURVE('',#14553,#14554,#8205,.T.) ;
#18563=EDGE_CURVE('',#14525,#14554,#686,.T.) ;
#18564=EDGE_CURVE('',#14554,#14524,#687,.T.) ;
#18565=EDGE_CURVE('',#14554,#14555,#8206,.T.) ;
#18566=EDGE_CURVE('',#14527,#14555,#688,.T.) ;
#18567=EDGE_CURVE('',#14555,#14526,#689,.T.) ;
#18568=EDGE_CURVE('',#14528,#14531,#8207,.T.) ;
#18569=EDGE_CURVE('',#14532,#14530,#690,.T.) ;
#18570=EDGE_CURVE('',#14533,#14535,#8208,.T.) ;
#18571=EDGE_CURVE('',#14536,#14534,#691,.T.) ;
#18572=EDGE_CURVE('',#14537,#14539,#8209,.T.) ;
#18573=EDGE_CURVE('',#14540,#14538,#692,.T.) ;
#18574=EDGE_CURVE('',#14541,#14543,#8210,.T.) ;
#18575=EDGE_CURVE('',#14544,#14542,#693,.T.) ;
#18576=EDGE_CURVE('',#14545,#14547,#8211,.T.) ;
#18577=EDGE_CURVE('',#14548,#14546,#694,.T.) ;
#18578=EDGE_CURVE('',#14549,#14556,#8212,.T.) ;
#18579=EDGE_CURVE('',#14557,#14556,#47,.T.) ;
#18580=EDGE_CURVE('',#14513,#14557,#695,.T.) ;
#18581=EDGE_CURVE('',#14558,#14515,#696,.T.) ;
#18582=EDGE_CURVE('',#14556,#14558,#48,.T.) ;
#18583=EDGE_CURVE('',#14517,#14559,#8213,.T.) ;
#18584=EDGE_CURVE('',#14551,#14559,#697,.T.) ;
#18585=EDGE_CURVE('',#14559,#14550,#698,.T.) ;
#18586=EDGE_CURVE('',#14559,#14552,#8214,.T.) ;
#18587=EDGE_CURVE('',#14514,#14558,#11852,.T.) ;
#18588=EDGE_CURVE('',#14556,#14560,#8215,.T.) ;
#18589=EDGE_CURVE('',#14560,#14560,#11853,.T.) ;
#18590=EDGE_CURVE('',#14557,#14512,#11854,.T.) ;
#26499=ORIENTED_EDGE('',*,*,#18515,.F.) ;
#26500=ORIENTED_EDGE('',*,*,#18516,.F.) ;
#26501=ORIENTED_EDGE('',*,*,#18517,.F.) ;
#26502=ORIENTED_EDGE('',*,*,#18518,.T.) ;
#26503=ORIENTED_EDGE('',*,*,#18519,.T.) ;
#26504=ORIENTED_EDGE('',*,*,#18520,.F.) ;
#26505=ORIENTED_EDGE('',*,*,#18521,.F.) ;
#26506=ORIENTED_EDGE('',*,*,#18522,.F.) ;
#26507=ORIENTED_EDGE('',*,*,#18519,.F.) ;
#26508=ORIENTED_EDGE('',*,*,#18523,.T.) ;
#26509=ORIENTED_EDGE('',*,*,#18524,.T.) ;
#26510=ORIENTED_EDGE('',*,*,#18525,.T.) ;
#26511=ORIENTED_EDGE('',*,*,#18526,.T.) ;
#26512=ORIENTED_EDGE('',*,*,#18527,.T.) ;
#26513=ORIENTED_EDGE('',*,*,#18528,.T.) ;
#26514=ORIENTED_EDGE('',*,*,#18529,.T.) ;
#26515=ORIENTED_EDGE('',*,*,#18530,.T.) ;
#26516=ORIENTED_EDGE('',*,*,#18531,.T.) ;
#26517=ORIENTED_EDGE('',*,*,#18532,.F.) ;
#26518=ORIENTED_EDGE('',*,*,#18532,.T.) ;
#26519=ORIENTED_EDGE('',*,*,#18533,.T.) ;
#26520=ORIENTED_EDGE('',*,*,#18534,.T.) ;
#26521=ORIENTED_EDGE('',*,*,#18535,.T.) ;
#26522=ORIENTED_EDGE('',*,*,#18536,.T.) ;
#26523=ORIENTED_EDGE('',*,*,#18537,.T.) ;
#26524=ORIENTED_EDGE('',*,*,#18538,.T.) ;
#26525=ORIENTED_EDGE('',*,*,#18539,.T.) ;
#26526=ORIENTED_EDGE('',*,*,#18540,.T.) ;
#26527=ORIENTED_EDGE('',*,*,#18541,.T.) ;
#26528=ORIENTED_EDGE('',*,*,#18542,.T.) ;
#26529=ORIENTED_EDGE('',*,*,#18543,.T.) ;
#26530=ORIENTED_EDGE('',*,*,#18544,.T.) ;
#26531=ORIENTED_EDGE('',*,*,#18545,.T.) ;
#26532=ORIENTED_EDGE('',*,*,#18546,.T.) ;
#26533=ORIENTED_EDGE('',*,*,#18547,.T.) ;
#26534=ORIENTED_EDGE('',*,*,#18548,.T.) ;
#26535=ORIENTED_EDGE('',*,*,#18549,.T.) ;
#26536=ORIENTED_EDGE('',*,*,#18550,.T.) ;
#26537=ORIENTED_EDGE('',*,*,#18551,.T.) ;
#26538=ORIENTED_EDGE('',*,*,#18552,.T.) ;
#26539=ORIENTED_EDGE('',*,*,#18553,.T.) ;
#26540=ORIENTED_EDGE('',*,*,#18521,.T.) ;
#26541=ORIENTED_EDGE('',*,*,#18554,.T.) ;
#26542=ORIENTED_EDGE('',*,*,#18555,.T.) ;
#26543=ORIENTED_EDGE('',*,*,#18556,.T.) ;
#26544=ORIENTED_EDGE('',*,*,#18557,.F.) ;
#26545=ORIENTED_EDGE('',*,*,#18524,.F.) ;
#26546=ORIENTED_EDGE('',*,*,#18558,.F.) ;
#26547=ORIENTED_EDGE('',*,*,#18559,.T.) ;
#26548=ORIENTED_EDGE('',*,*,#18560,.F.) ;
#26549=ORIENTED_EDGE('',*,*,#18526,.F.) ;
#26550=ORIENTED_EDGE('',*,*,#18561,.F.) ;
#26551=ORIENTED_EDGE('',*,*,#18559,.F.) ;
#26552=ORIENTED_EDGE('',*,*,#18560,.T.) ;
#26553=ORIENTED_EDGE('',*,*,#18562,.T.) ;
#26554=ORIENTED_EDGE('',*,*,#18563,.F.) ;
#26555=ORIENTED_EDGE('',*,*,#18528,.F.) ;
#26556=ORIENTED_EDGE('',*,*,#18564,.F.) ;
#26557=ORIENTED_EDGE('',*,*,#18562,.F.) ;
#26558=ORIENTED_EDGE('',*,*,#18561,.T.) ;
#26559=ORIENTED_EDGE('',*,*,#18527,.F.) ;
#26560=ORIENTED_EDGE('',*,*,#18563,.T.) ;
#26561=ORIENTED_EDGE('',*,*,#18565,.T.) ;
#26562=ORIENTED_EDGE('',*,*,#18566,.F.) ;
#26563=ORIENTED_EDGE('',*,*,#18530,.F.) ;
#26564=ORIENTED_EDGE('',*,*,#18567,.F.) ;
#26565=ORIENTED_EDGE('',*,*,#18565,.F.) ;
#26566=ORIENTED_EDGE('',*,*,#18564,.T.) ;
#26567=ORIENTED_EDGE('',*,*,#18529,.F.) ;
#26568=ORIENTED_EDGE('',*,*,#18566,.T.) ;
#26569=ORIENTED_EDGE('',*,*,#18567,.T.) ;
#26570=ORIENTED_EDGE('',*,*,#18533,.F.) ;
#26571=ORIENTED_EDGE('',*,*,#18568,.T.) ;
#26572=ORIENTED_EDGE('',*,*,#18534,.F.) ;
#26573=ORIENTED_EDGE('',*,*,#18569,.F.) ;
#26574=ORIENTED_EDGE('',*,*,#18535,.F.) ;
#26575=ORIENTED_EDGE('',*,*,#18568,.F.) ;
#26576=ORIENTED_EDGE('',*,*,#18531,.F.) ;
#26577=ORIENTED_EDGE('',*,*,#18569,.T.) ;
#26578=ORIENTED_EDGE('',*,*,#18537,.F.) ;
#26579=ORIENTED_EDGE('',*,*,#18570,.T.) ;
#26580=ORIENTED_EDGE('',*,*,#18538,.F.) ;
#26581=ORIENTED_EDGE('',*,*,#18571,.F.) ;
#26582=ORIENTED_EDGE('',*,*,#18539,.F.) ;
#26583=ORIENTED_EDGE('',*,*,#18570,.F.) ;
#26584=ORIENTED_EDGE('',*,*,#18536,.F.) ;
#26585=ORIENTED_EDGE('',*,*,#18571,.T.) ;
#26586=ORIENTED_EDGE('',*,*,#18541,.F.) ;
#26587=ORIENTED_EDGE('',*,*,#18572,.T.) ;
#26588=ORIENTED_EDGE('',*,*,#18542,.F.) ;
#26589=ORIENTED_EDGE('',*,*,#18573,.F.) ;
#26590=ORIENTED_EDGE('',*,*,#18543,.F.) ;
#26591=ORIENTED_EDGE('',*,*,#18572,.F.) ;
#26592=ORIENTED_EDGE('',*,*,#18540,.F.) ;
#26593=ORIENTED_EDGE('',*,*,#18573,.T.) ;
#26594=ORIENTED_EDGE('',*,*,#18545,.F.) ;
#26595=ORIENTED_EDGE('',*,*,#18574,.T.) ;
#26596=ORIENTED_EDGE('',*,*,#18546,.F.) ;
#26597=ORIENTED_EDGE('',*,*,#18575,.F.) ;
#26598=ORIENTED_EDGE('',*,*,#18547,.F.) ;
#26599=ORIENTED_EDGE('',*,*,#18574,.F.) ;
#26600=ORIENTED_EDGE('',*,*,#18544,.F.) ;
#26601=ORIENTED_EDGE('',*,*,#18575,.T.) ;
#26602=ORIENTED_EDGE('',*,*,#18549,.F.) ;
#26603=ORIENTED_EDGE('',*,*,#18576,.T.) ;
#26604=ORIENTED_EDGE('',*,*,#18550,.F.) ;
#26605=ORIENTED_EDGE('',*,*,#18577,.F.) ;
#26606=ORIENTED_EDGE('',*,*,#18551,.F.) ;
#26607=ORIENTED_EDGE('',*,*,#18576,.F.) ;
#26608=ORIENTED_EDGE('',*,*,#18548,.F.) ;
#26609=ORIENTED_EDGE('',*,*,#18577,.T.) ;
#26610=ORIENTED_EDGE('',*,*,#18553,.F.) ;
#26611=ORIENTED_EDGE('',*,*,#18578,.T.) ;
#26612=ORIENTED_EDGE('',*,*,#18579,.F.) ;
#26613=ORIENTED_EDGE('',*,*,#18580,.F.) ;
#26614=ORIENTED_EDGE('',*,*,#18523,.F.) ;
#26615=ORIENTED_EDGE('',*,*,#18518,.F.) ;
#26616=ORIENTED_EDGE('',*,*,#18581,.F.) ;
#26617=ORIENTED_EDGE('',*,*,#18582,.F.) ;
#26618=ORIENTED_EDGE('',*,*,#18578,.F.) ;
#26619=ORIENTED_EDGE('',*,*,#18552,.F.) ;
#26620=ORIENTED_EDGE('',*,*,#18520,.T.) ;
#26621=ORIENTED_EDGE('',*,*,#18583,.T.) ;
#26622=ORIENTED_EDGE('',*,*,#18584,.F.) ;
#26623=ORIENTED_EDGE('',*,*,#18555,.F.) ;
#26624=ORIENTED_EDGE('',*,*,#18585,.F.) ;
#26625=ORIENTED_EDGE('',*,*,#18583,.F.) ;
#26626=ORIENTED_EDGE('',*,*,#18522,.T.) ;
#26627=ORIENTED_EDGE('',*,*,#18554,.F.) ;
#26628=ORIENTED_EDGE('',*,*,#18584,.T.) ;
#26629=ORIENTED_EDGE('',*,*,#18586,.T.) ;
#26630=ORIENTED_EDGE('',*,*,#18558,.T.) ;
#26631=ORIENTED_EDGE('',*,*,#18525,.F.) ;
#26632=ORIENTED_EDGE('',*,*,#18557,.T.) ;
#26633=ORIENTED_EDGE('',*,*,#18586,.F.) ;
#26634=ORIENTED_EDGE('',*,*,#18585,.T.) ;
#26635=ORIENTED_EDGE('',*,*,#18556,.F.) ;
#26636=ORIENTED_EDGE('',*,*,#18581,.T.) ;
#26637=ORIENTED_EDGE('',*,*,#18517,.T.) ;
#26638=ORIENTED_EDGE('',*,*,#18587,.T.) ;
#26639=ORIENTED_EDGE('',*,*,#18579,.T.) ;
#26640=ORIENTED_EDGE('',*,*,#18588,.T.) ;
#26641=ORIENTED_EDGE('',*,*,#18589,.F.) ;
#26642=ORIENTED_EDGE('',*,*,#18588,.F.) ;
#26643=ORIENTED_EDGE('',*,*,#18582,.T.) ;
#26644=ORIENTED_EDGE('',*,*,#18587,.F.) ;
#26645=ORIENTED_EDGE('',*,*,#18516,.T.) ;
#26646=ORIENTED_EDGE('',*,*,#18590,.F.) ;
#26647=ORIENTED_EDGE('',*,*,#18589,.T.) ;
#26648=ORIENTED_EDGE('',*,*,#18580,.T.) ;
#26649=ORIENTED_EDGE('',*,*,#18590,.T.) ;
#26650=ORIENTED_EDGE('',*,*,#18515,.T.) ;
#27062=CYLINDRICAL_SURFACE('',#32278,0.25) ;
#27063=CYLINDRICAL_SURFACE('',#32330,0.25) ;
#27064=CYLINDRICAL_SURFACE('',#32335,0.25) ;
#27065=CYLINDRICAL_SURFACE('',#32338,0.25) ;
#27066=CYLINDRICAL_SURFACE('',#32341,0.25) ;
#27067=CYLINDRICAL_SURFACE('',#32343,0.25) ;
#27068=CYLINDRICAL_SURFACE('',#32345,0.25) ;
#27069=CYLINDRICAL_SURFACE('',#32347,0.25) ;
#27070=CYLINDRICAL_SURFACE('',#32349,0.25) ;
#27071=CYLINDRICAL_SURFACE('',#32351,0.25) ;
#27072=CYLINDRICAL_SURFACE('',#32354,0.25) ;
#27073=CYLINDRICAL_SURFACE('',#32357,0.25) ;
#27074=CYLINDRICAL_SURFACE('',#32360,0.3) ;
#28602=ADVANCED_FACE('',(#3867),#27062,.T.) ;
#28603=ADVANCED_FACE('',(#3868),#880,.T.) ;
#28604=ADVANCED_FACE('',(#3869),#881,.T.) ;
#28605=ADVANCED_FACE('',(#3870),#882,.T.) ;
#28606=ADVANCED_FACE('',(#3871),#883,.T.) ;
#28607=ADVANCED_FACE('',(#3872),#884,.T.) ;
#28608=ADVANCED_FACE('',(#3873),#885,.T.) ;
#28609=ADVANCED_FACE('',(#3874),#886,.T.) ;
#28610=ADVANCED_FACE('',(#3875),#887,.T.) ;
#28611=ADVANCED_FACE('',(#3876),#888,.T.) ;
#28612=ADVANCED_FACE('',(#3877),#889,.T.) ;
#28613=ADVANCED_FACE('',(#3878),#890,.T.) ;
#28614=ADVANCED_FACE('',(#3879),#27063,.T.) ;
#28615=ADVANCED_FACE('',(#3880),#27064,.T.) ;
#28616=ADVANCED_FACE('',(#3881),#27065,.T.) ;
#28617=ADVANCED_FACE('',(#3882),#27066,.T.) ;
#28618=ADVANCED_FACE('',(#3883),#27067,.T.) ;
#28619=ADVANCED_FACE('',(#3884),#27068,.T.) ;
#28620=ADVANCED_FACE('',(#3885),#27069,.T.) ;
#28621=ADVANCED_FACE('',(#3886),#27070,.T.) ;
#28622=ADVANCED_FACE('',(#3887),#27071,.T.) ;
#28623=ADVANCED_FACE('',(#3888),#27072,.T.) ;
#28624=ADVANCED_FACE('',(#3889),#27073,.T.) ;
#28625=ADVANCED_FACE('',(#3890),#2337,.T.) ;
#28626=ADVANCED_FACE('',(#3891),#27074,.T.) ;
#28627=ADVANCED_FACE('',(#3892),#2338,.T.) ;
#28628=ADVANCED_FACE('',(#3893),#2339,.T.) ;
#28714=CLOSED_SHELL('',(#28602,#28603,#28604,#28605,#28606,#28607,#28608,
#28609,#28610,#28611,#28612,#28613,#28614,#28615,#28616,#28617,#28618,#28619,
#28620,#28621,#28622,#28623,#28624,#28625,#28626,#28627,#28628)) ;
#32277=AXIS2_PLACEMENT_3D('',#50113,#40982,#40983) ;
#32278=AXIS2_PLACEMENT_3D('',#50114,#40984,#40985) ;
#32279=AXIS2_PLACEMENT_3D('',#50117,#40986,#40987) ;
#32280=AXIS2_PLACEMENT_3D('',#50142,#40988,#40989) ;
#32281=AXIS2_PLACEMENT_3D('',#50144,#40990,#40991) ;
#32282=AXIS2_PLACEMENT_3D('',#50148,#40993,#40994) ;
#32283=AXIS2_PLACEMENT_3D('',#50150,#40995,#40996) ;
#32284=AXIS2_PLACEMENT_3D('',#50151,#40997,#40998) ;
#32285=AXIS2_PLACEMENT_3D('',#50152,#40999,#41000) ;
#32286=AXIS2_PLACEMENT_3D('',#50153,#41001,#41002) ;
#32287=AXIS2_PLACEMENT_3D('',#50156,#41003,#41004) ;
#32288=AXIS2_PLACEMENT_3D('',#50157,#41005,#41006) ;
#32289=AXIS2_PLACEMENT_3D('',#50158,#41007,#41008) ;
#32290=AXIS2_PLACEMENT_3D('',#50161,#41009,#41010) ;
#32291=AXIS2_PLACEMENT_3D('',#50162,#41011,#41012) ;
#32292=AXIS2_PLACEMENT_3D('',#50163,#41013,#41014) ;
#32293=AXIS2_PLACEMENT_3D('',#50166,#41015,#41016) ;
#32294=AXIS2_PLACEMENT_3D('',#50167,#41017,#41018) ;
#32295=AXIS2_PLACEMENT_3D('',#50168,#41019,#41020) ;
#32296=AXIS2_PLACEMENT_3D('',#50171,#41021,#41022) ;
#32297=AXIS2_PLACEMENT_3D('',#50173,#41023,#41024) ;
#32298=AXIS2_PLACEMENT_3D('',#50175,#41025,#41026) ;
#32299=AXIS2_PLACEMENT_3D('',#50176,#41027,#41028) ;
#32300=AXIS2_PLACEMENT_3D('',#50177,#41029,#41030) ;
#32301=AXIS2_PLACEMENT_3D('',#50180,#41031,#41032) ;
#32302=AXIS2_PLACEMENT_3D('',#50182,#41033,#41034) ;
#32303=AXIS2_PLACEMENT_3D('',#50184,#41035,#41036) ;
#32304=AXIS2_PLACEMENT_3D('',#50185,#41037,#41038) ;
#32305=AXIS2_PLACEMENT_3D('',#50186,#41039,#41040) ;
#32306=AXIS2_PLACEMENT_3D('',#50189,#41041,#41042) ;
#32307=AXIS2_PLACEMENT_3D('',#50191,#41043,#41044) ;
#32308=AXIS2_PLACEMENT_3D('',#50193,#41045,#41046) ;
#32309=AXIS2_PLACEMENT_3D('',#50194,#41047,#41048) ;
#32310=AXIS2_PLACEMENT_3D('',#50195,#41049,#41050) ;
#32311=AXIS2_PLACEMENT_3D('',#50198,#41051,#41052) ;
#32312=AXIS2_PLACEMENT_3D('',#50200,#41053,#41054) ;
#32313=AXIS2_PLACEMENT_3D('',#50202,#41055,#41056) ;
#32314=AXIS2_PLACEMENT_3D('',#50203,#41057,#41058) ;
#32315=AXIS2_PLACEMENT_3D('',#50204,#41059,#41060) ;
#32316=AXIS2_PLACEMENT_3D('',#50207,#41061,#41062) ;
#32317=AXIS2_PLACEMENT_3D('',#50209,#41063,#41064) ;
#32318=AXIS2_PLACEMENT_3D('',#50211,#41065,#41066) ;
#32319=AXIS2_PLACEMENT_3D('',#50212,#41067,#41068) ;
#32320=AXIS2_PLACEMENT_3D('',#50213,#41069,#41070) ;
#32321=AXIS2_PLACEMENT_3D('',#50216,#41071,#41072) ;
#32322=AXIS2_PLACEMENT_3D('',#50218,#41073,#41074) ;
#32323=AXIS2_PLACEMENT_3D('',#50220,#41075,#41076) ;
#32324=AXIS2_PLACEMENT_3D('',#50221,#41077,#41078) ;
#32325=AXIS2_PLACEMENT_3D('',#50222,#41079,#41080) ;
#32326=AXIS2_PLACEMENT_3D('',#50223,#41081,#41082) ;
#32327=AXIS2_PLACEMENT_3D('',#50224,#41083,#41084) ;
#32328=AXIS2_PLACEMENT_3D('',#50227,#41085,#41086) ;
#32329=AXIS2_PLACEMENT_3D('',#50228,#41087,#41088) ;
#32330=AXIS2_PLACEMENT_3D('',#50229,#41089,#41090) ;
#32331=AXIS2_PLACEMENT_3D('',#50231,#41091,#41092) ;
#32332=AXIS2_PLACEMENT_3D('',#50232,#41093,#41094) ;
#32333=AXIS2_PLACEMENT_3D('',#50235,#41096,#41097) ;
#32334=AXIS2_PLACEMENT_3D('',#50236,#41098,#41099) ;
#32335=AXIS2_PLACEMENT_3D('',#50237,#41100,#41101) ;
#32336=AXIS2_PLACEMENT_3D('',#50240,#41103,#41104) ;
#32337=AXIS2_PLACEMENT_3D('',#50241,#41105,#41106) ;
#32338=AXIS2_PLACEMENT_3D('',#50242,#41107,#41108) ;
#32339=AXIS2_PLACEMENT_3D('',#50245,#41110,#41111) ;
#32340=AXIS2_PLACEMENT_3D('',#50246,#41112,#41113) ;
#32341=AXIS2_PLACEMENT_3D('',#50247,#41114,#41115) ;
#32342=AXIS2_PLACEMENT_3D('',#50249,#41117,#41118) ;
#32343=AXIS2_PLACEMENT_3D('',#50250,#41119,#41120) ;
#32344=AXIS2_PLACEMENT_3D('',#50252,#41122,#41123) ;
#32345=AXIS2_PLACEMENT_3D('',#50253,#41124,#41125) ;
#32346=AXIS2_PLACEMENT_3D('',#50255,#41127,#41128) ;
#32347=AXIS2_PLACEMENT_3D('',#50256,#41129,#41130) ;
#32348=AXIS2_PLACEMENT_3D('',#50258,#41132,#41133) ;
#32349=AXIS2_PLACEMENT_3D('',#50259,#41134,#41135) ;
#32350=AXIS2_PLACEMENT_3D('',#50261,#41137,#41138) ;
#32351=AXIS2_PLACEMENT_3D('',#50262,#41139,#41140) ;
#32352=AXIS2_PLACEMENT_3D('',#50278,#41142,#41143) ;
#32353=AXIS2_PLACEMENT_3D('',#50280,#41144,#41145) ;
#32354=AXIS2_PLACEMENT_3D('',#50293,#41146,#41147) ;
#32355=AXIS2_PLACEMENT_3D('',#50296,#41149,#41150) ;
#32356=AXIS2_PLACEMENT_3D('',#50297,#41151,#41152) ;
#32357=AXIS2_PLACEMENT_3D('',#50298,#41153,#41154) ;
#32358=AXIS2_PLACEMENT_3D('',#50300,#41156,#41157) ;
#32359=AXIS2_PLACEMENT_3D('',#50301,#41158,#41159) ;
#32360=AXIS2_PLACEMENT_3D('',#50302,#41160,#41161) ;
#32361=AXIS2_PLACEMENT_3D('',#50305,#41163,#41164) ;
#32362=AXIS2_PLACEMENT_3D('',#50306,#41165,#41166) ;
#32363=AXIS2_PLACEMENT_3D('',#50307,#41167,#41168) ;
#32364=AXIS2_PLACEMENT_3D('',#50308,#41169,#41170) ;
#40982=DIRECTION('axis',(0.,0.,1.)) ;
#40983=DIRECTION('refdir',(1.,0.,0.)) ;
#40984=DIRECTION('center_axis',(-0.965925826289068,0.,-0.258819045102521)) ;
#40985=DIRECTION('ref_axis',(0.258819045102521,0.,-0.965925826289068)) ;
#40986=DIRECTION('center_axis',(0.,0.,-1.)) ;
#40987=DIRECTION('ref_axis',(1.,0.,0.)) ;
#40988=DIRECTION('center_axis',(0.,0.,-1.)) ;
#40989=DIRECTION('ref_axis',(1.,0.,0.)) ;
#40990=DIRECTION('center_axis',(1.,0.,-2.14478618485241E-16)) ;
#40991=DIRECTION('ref_axis',(2.14478618485241E-16,0.,1.)) ;
#40992=DIRECTION('',(0.965925826289068,0.,0.258819045102521)) ;
#40993=DIRECTION('center_axis',(0.866025403784437,0.,0.500000000000003)) ;
#40994=DIRECTION('ref_axis',(0.500000000000003,0.,-0.866025403784437)) ;
#40995=DIRECTION('center_axis',(0.965925826289068,0.,0.258819045102521)) ;
#40996=DIRECTION('ref_axis',(0.258819045102521,0.,-0.965925826289068)) ;
#40997=DIRECTION('center_axis',(0.866025403784437,0.,0.500000000000003)) ;
#40998=DIRECTION('ref_axis',(0.500000000000003,0.,-0.866025403784437)) ;
#40999=DIRECTION('center_axis',(1.,0.,-2.14478618485241E-16)) ;
#41000=DIRECTION('ref_axis',(2.14478618485241E-16,0.,1.)) ;
#41001=DIRECTION('center_axis',(0.,0.,1.)) ;
#41002=DIRECTION('ref_axis',(1.,0.,0.)) ;
#41003=DIRECTION('center_axis',(0.258819045102521,0.,-0.965925826289068)) ;
#41004=DIRECTION('ref_axis',(0.965925826289068,0.,0.258819045102521)) ;
#41005=DIRECTION('center_axis',(0.25881904510252,0.,0.965925826289068)) ;
#41006=DIRECTION('ref_axis',(0.965925826289068,0.,-0.25881904510252)) ;
#41007=DIRECTION('center_axis',(0.,0.,1.)) ;
#41008=DIRECTION('ref_axis',(1.,0.,0.)) ;
#41009=DIRECTION('center_axis',(-0.258819045102521,0.,0.965925826289068)) ;
#41010=DIRECTION('ref_axis',(0.965925826289068,0.,0.258819045102521)) ;
#41011=DIRECTION('center_axis',(0.707106781186548,0.,-0.707106781186547)) ;
#41012=DIRECTION('ref_axis',(0.707106781186547,0.,0.707106781186548)) ;
#41013=DIRECTION('center_axis',(0.,0.,1.)) ;
#41014=DIRECTION('ref_axis',(1.,0.,0.)) ;
#41015=DIRECTION('center_axis',(-0.707106781186548,0.,0.707106781186547)) ;
#41016=DIRECTION('ref_axis',(0.707106781186547,0.,0.707106781186548)) ;
#41017=DIRECTION('center_axis',(0.965925826289068,0.,-0.258819045102522)) ;
#41018=DIRECTION('ref_axis',(0.258819045102522,0.,0.965925826289068)) ;
#41019=DIRECTION('center_axis',(6.12323399573676E-17,0.,1.)) ;
#41020=DIRECTION('ref_axis',(1.,0.,0.)) ;
#41021=DIRECTION('center_axis',(-0.965925826289068,0.,0.258819045102522)) ;
#41022=DIRECTION('ref_axis',(0.258819045102522,0.,0.965925826289068)) ;
#41023=DIRECTION('center_axis',(0.965925826289068,0.,0.258819045102522)) ;
#41024=DIRECTION('ref_axis',(0.258819045102522,0.,-0.965925826289068)) ;
#41025=DIRECTION('center_axis',(1.22464679914735E-16,-1.,0.)) ;
#41026=DIRECTION('ref_axis',(-1.,-1.22464679914735E-16,0.)) ;
#41027=DIRECTION('center_axis',(0.965925826289068,0.,0.258819045102522)) ;
#41028=DIRECTION('ref_axis',(0.258819045102522,0.,-0.965925826289068)) ;
#41029=DIRECTION('center_axis',(0.,-7.49879891330929E-33,1.)) ;
#41030=DIRECTION('ref_axis',(-1.,-1.22464679914735E-16,0.)) ;
#41031=DIRECTION('center_axis',(-0.965925826289068,0.,-0.258819045102522)) ;
#41032=DIRECTION('ref_axis',(0.258819045102522,0.,-0.965925826289068)) ;
#41033=DIRECTION('center_axis',(-0.965925826289068,0.,-0.258819045102522)) ;
#41034=DIRECTION('ref_axis',(0.258819045102522,0.,-0.965925826289068)) ;
#41035=DIRECTION('center_axis',(0.707106781186548,0.,0.707106781186547)) ;
#41036=DIRECTION('ref_axis',(0.707106781186547,0.,-0.707106781186548)) ;
#41037=DIRECTION('center_axis',(0.707106781186548,0.,0.707106781186547)) ;
#41038=DIRECTION('ref_axis',(0.707106781186547,0.,-0.707106781186548)) ;
#41039=DIRECTION('center_axis',(0.,-7.49879891330929E-33,1.)) ;
#41040=DIRECTION('ref_axis',(-1.,-1.22464679914735E-16,0.)) ;
#41041=DIRECTION('center_axis',(-0.707106781186548,0.,-0.707106781186547)) ;
#41042=DIRECTION('ref_axis',(0.707106781186547,0.,-0.707106781186548)) ;
#41043=DIRECTION('center_axis',(-0.707106781186548,0.,-0.707106781186547)) ;
#41044=DIRECTION('ref_axis',(0.707106781186547,0.,-0.707106781186548)) ;
#41045=DIRECTION('center_axis',(0.25881904510252,0.,0.965925826289068)) ;
#41046=DIRECTION('ref_axis',(0.965925826289068,0.,-0.25881904510252)) ;
#41047=DIRECTION('center_axis',(0.25881904510252,0.,0.965925826289068)) ;
#41048=DIRECTION('ref_axis',(0.965925826289068,0.,-0.25881904510252)) ;
#41049=DIRECTION('center_axis',(0.,-7.49879891330929E-33,1.)) ;
#41050=DIRECTION('ref_axis',(-1.,-1.22464679914735E-16,0.)) ;
#41051=DIRECTION('center_axis',(-0.25881904510252,0.,-0.965925826289068)) ;
#41052=DIRECTION('ref_axis',(0.965925826289068,0.,-0.25881904510252)) ;
#41053=DIRECTION('center_axis',(-0.25881904510252,0.,-0.965925826289068)) ;
#41054=DIRECTION('ref_axis',(0.965925826289068,0.,-0.25881904510252)) ;
#41055=DIRECTION('center_axis',(-0.25881904510252,0.,0.965925826289068)) ;
#41056=DIRECTION('ref_axis',(0.965925826289068,0.,0.25881904510252)) ;
#41057=DIRECTION('center_axis',(-0.25881904510252,0.,0.965925826289068)) ;
#41058=DIRECTION('ref_axis',(0.965925826289068,0.,0.25881904510252)) ;
#41059=DIRECTION('center_axis',(0.,-7.49879891330929E-33,1.)) ;
#41060=DIRECTION('ref_axis',(-1.,-1.22464679914735E-16,0.)) ;
#41061=DIRECTION('center_axis',(0.25881904510252,0.,-0.965925826289068)) ;
#41062=DIRECTION('ref_axis',(0.965925826289068,0.,0.25881904510252)) ;
#41063=DIRECTION('center_axis',(0.25881904510252,0.,-0.965925826289068)) ;
#41064=DIRECTION('ref_axis',(0.965925826289068,0.,0.25881904510252)) ;
#41065=DIRECTION('center_axis',(-0.707106781186547,0.,0.707106781186548)) ;
#41066=DIRECTION('ref_axis',(0.707106781186548,0.,0.707106781186547)) ;
#41067=DIRECTION('center_axis',(-0.707106781186547,0.,0.707106781186548)) ;
#41068=DIRECTION('ref_axis',(0.707106781186548,0.,0.707106781186547)) ;
#41069=DIRECTION('center_axis',(0.,-7.49879891330928E-33,1.)) ;
#41070=DIRECTION('ref_axis',(-1.,-1.22464679914735E-16,0.)) ;
#41071=DIRECTION('center_axis',(0.707106781186547,0.,-0.707106781186548)) ;
#41072=DIRECTION('ref_axis',(0.707106781186548,0.,0.707106781186547)) ;
#41073=DIRECTION('center_axis',(0.707106781186547,0.,-0.707106781186548)) ;
#41074=DIRECTION('ref_axis',(0.707106781186548,0.,0.707106781186547)) ;
#41075=DIRECTION('center_axis',(-0.965925826289068,0.,0.258819045102521)) ;
#41076=DIRECTION('ref_axis',(0.258819045102521,0.,0.965925826289068)) ;
#41077=DIRECTION('center_axis',(-0.965925826289068,0.,0.258819045102521)) ;
#41078=DIRECTION('ref_axis',(0.258819045102521,0.,0.965925826289068)) ;
#41079=DIRECTION('center_axis',(0.,0.,1.)) ;
#41080=DIRECTION('ref_axis',(1.,0.,0.)) ;
#41081=DIRECTION('center_axis',(-0.707106781186547,0.,-0.707106781186548)) ;
#41082=DIRECTION('ref_axis',(0.707106781186548,0.,-0.707106781186547)) ;
#41083=DIRECTION('center_axis',(0.,0.,1.)) ;
#41084=DIRECTION('ref_axis',(1.,0.,0.)) ;
#41085=DIRECTION('center_axis',(0.707106781186547,0.,0.707106781186548)) ;
#41086=DIRECTION('ref_axis',(0.707106781186548,0.,-0.707106781186547)) ;
#41087=DIRECTION('center_axis',(-0.25881904510252,0.,-0.965925826289068)) ;
#41088=DIRECTION('ref_axis',(0.965925826289068,0.,-0.25881904510252)) ;
#41089=DIRECTION('center_axis',(0.258819045102521,0.,-0.965925826289068)) ;
#41090=DIRECTION('ref_axis',(0.965925826289068,0.,0.258819045102521)) ;
#41091=DIRECTION('center_axis',(1.71582894788192E-15,0.,-1.)) ;
#41092=DIRECTION('ref_axis',(1.,0.,1.71582894788193E-15)) ;
#41093=DIRECTION('center_axis',(1.71582894788192E-15,0.,-1.)) ;
#41094=DIRECTION('ref_axis',(1.,0.,1.71582894788193E-15)) ;
#41095=DIRECTION('',(-0.258819045102521,0.,0.965925826289068)) ;
#41096=DIRECTION('center_axis',(-0.500000000000002,0.,0.866025403784438)) ;
#41097=DIRECTION('ref_axis',(0.866025403784438,0.,0.500000000000002)) ;
#41098=DIRECTION('center_axis',(-0.500000000000002,0.,0.866025403784438)) ;
#41099=DIRECTION('ref_axis',(0.866025403784438,0.,0.500000000000002)) ;
#41100=DIRECTION('center_axis',(0.707106781186548,0.,-0.707106781186547)) ;
#41101=DIRECTION('ref_axis',(0.707106781186547,0.,0.707106781186548)) ;
#41102=DIRECTION('',(-0.707106781186548,0.,0.707106781186547)) ;
#41103=DIRECTION('center_axis',(-0.866025403784438,0.,0.500000000000001)) ;
#41104=DIRECTION('ref_axis',(0.500000000000001,0.,0.866025403784438)) ;
#41105=DIRECTION('center_axis',(-0.866025403784438,0.,0.500000000000001)) ;
#41106=DIRECTION('ref_axis',(0.500000000000001,0.,0.866025403784438)) ;
#41107=DIRECTION('center_axis',(0.965925826289068,0.,-0.258819045102522)) ;
#41108=DIRECTION('ref_axis',(0.258819045102522,0.,0.965925826289068)) ;
#41109=DIRECTION('',(-0.965925826289068,0.,0.258819045102522)) ;
#41110=DIRECTION('center_axis',(-1.,0.,3.21717927727861E-16)) ;
#41111=DIRECTION('ref_axis',(3.75337582349171E-16,0.,1.)) ;
#41112=DIRECTION('center_axis',(-1.,0.,3.21717927727861E-16)) ;
#41113=DIRECTION('ref_axis',(3.75337582349171E-16,0.,1.)) ;
#41114=DIRECTION('center_axis',(0.965925826289068,0.,0.258819045102522)) ;
#41115=DIRECTION('ref_axis',(0.258819045102522,0.,-0.965925826289068)) ;
#41116=DIRECTION('',(-0.965925826289068,0.,-0.258819045102522)) ;
#41117=DIRECTION('center_axis',(-0.866025403784437,0.,-0.500000000000002)) ;
#41118=DIRECTION('ref_axis',(0.500000000000002,0.,-0.866025403784437)) ;
#41119=DIRECTION('center_axis',(0.707106781186548,0.,0.707106781186547)) ;
#41120=DIRECTION('ref_axis',(0.707106781186547,0.,-0.707106781186548)) ;
#41121=DIRECTION('',(-0.707106781186548,0.,-0.707106781186547)) ;
#41122=DIRECTION('center_axis',(-0.500000000000002,0.,-0.866025403784438)) ;
#41123=DIRECTION('ref_axis',(0.866025403784438,0.,-0.500000000000002)) ;
#41124=DIRECTION('center_axis',(0.25881904510252,0.,0.965925826289068)) ;
#41125=DIRECTION('ref_axis',(0.965925826289068,0.,-0.25881904510252)) ;
#41126=DIRECTION('',(-0.25881904510252,0.,-0.965925826289068)) ;
#41127=DIRECTION('center_axis',(0.,0.,-1.)) ;
#41128=DIRECTION('ref_axis',(1.,0.,0.)) ;
#41129=DIRECTION('center_axis',(-0.25881904510252,0.,0.965925826289068)) ;
#41130=DIRECTION('ref_axis',(0.965925826289068,0.,0.25881904510252)) ;
#41131=DIRECTION('',(0.25881904510252,0.,-0.965925826289068)) ;
#41132=DIRECTION('center_axis',(0.5,0.,-0.866025403784439)) ;
#41133=DIRECTION('ref_axis',(0.866025403784439,0.,0.5)) ;
#41134=DIRECTION('center_axis',(-0.707106781186547,0.,0.707106781186548)) ;
#41135=DIRECTION('ref_axis',(0.707106781186548,0.,0.707106781186547)) ;
#41136=DIRECTION('',(0.707106781186547,0.,-0.707106781186548)) ;
#41137=DIRECTION('center_axis',(0.866025403784439,0.,-0.499999999999999)) ;
#41138=DIRECTION('ref_axis',(0.499999999999999,0.,0.866025403784439)) ;
#41139=DIRECTION('center_axis',(-0.965925826289068,0.,0.258819045102521)) ;
#41140=DIRECTION('ref_axis',(0.258819045102521,0.,0.965925826289068)) ;
#41141=DIRECTION('',(0.965925826289068,0.,-0.258819045102521)) ;
#41142=DIRECTION('center_axis',(0.,0.,-1.)) ;
#41143=DIRECTION('ref_axis',(1.,0.,0.)) ;
#41144=DIRECTION('center_axis',(0.,0.,-1.)) ;
#41145=DIRECTION('ref_axis',(1.,0.,0.)) ;
#41146=DIRECTION('center_axis',(-0.707106781186547,0.,-0.707106781186548)) ;
#41147=DIRECTION('ref_axis',(0.707106781186548,0.,-0.707106781186547)) ;
#41148=DIRECTION('',(0.707106781186547,0.,0.707106781186548)) ;
#41149=DIRECTION('center_axis',(0.500000000000001,0.,0.866025403784438)) ;
#41150=DIRECTION('ref_axis',(0.866025403784438,0.,-0.500000000000001)) ;
#41151=DIRECTION('center_axis',(0.500000000000001,0.,0.866025403784438)) ;
#41152=DIRECTION('ref_axis',(0.866025403784438,0.,-0.500000000000001)) ;
#41153=DIRECTION('center_axis',(-0.25881904510252,0.,-0.965925826289068)) ;
#41154=DIRECTION('ref_axis',(0.965925826289068,0.,-0.25881904510252)) ;
#41155=DIRECTION('',(0.25881904510252,0.,0.965925826289068)) ;
#41156=DIRECTION('center_axis',(0.,0.,1.)) ;
#41157=DIRECTION('ref_axis',(1.,0.,0.)) ;
#41158=DIRECTION('center_axis',(0.,0.,1.)) ;
#41159=DIRECTION('ref_axis',(1.,0.,0.)) ;
#41160=DIRECTION('center_axis',(0.,0.,1.)) ;
#41161=DIRECTION('ref_axis',(1.,0.,0.)) ;
#41162=DIRECTION('',(0.,0.,-1.)) ;
#41163=DIRECTION('center_axis',(0.,0.,-1.)) ;
#41164=DIRECTION('ref_axis',(1.,0.,0.)) ;
#41165=DIRECTION('center_axis',(0.,0.,1.)) ;
#41166=DIRECTION('ref_axis',(1.,0.,0.)) ;
#41167=DIRECTION('center_axis',(0.,0.,-1.)) ;
#41168=DIRECTION('ref_axis',(-1.,0.,0.)) ;
#41169=DIRECTION('center_axis',(0.,0.,1.)) ;
#41170=DIRECTION('ref_axis',(1.,0.,0.)) ;
#50113=CARTESIAN_POINT('',(0.,0.,0.)) ;
#50114=CARTESIAN_POINT('Origin',(0.25,0.,1.86698729810778)) ;
#50115=CARTESIAN_POINT('',(0.171681132240627,-0.246019488725134,1.8)) ;
#50116=CARTESIAN_POINT('',(1.64540693022728E-16,-0.25,1.8)) ;
#50117=CARTESIAN_POINT('Origin',(5.27355936696949E-16,0.,1.8)) ;
#50118=CARTESIAN_POINT('',(0.171681132240627,0.246019488725134,1.8)) ;
#50119=CARTESIAN_POINT('Ctrl Pts',(0.171681132240627,0.246019488725134,
1.8)) ;
#50120=CARTESIAN_POINT('Ctrl Pts',(0.171928929654082,0.245846566893906,
1.799075207463)) ;
#50121=CARTESIAN_POINT('Ctrl Pts',(0.172184099341621,0.24566794421234,1.79815279520613)) ;
#50122=CARTESIAN_POINT('Ctrl Pts',(0.176787603683127,0.242434088321297,
1.782012704586)) ;
#50123=CARTESIAN_POINT('Ctrl Pts',(0.183141637145544,0.237803273510375,
1.76748264287115)) ;
#50124=CARTESIAN_POINT('Ctrl Pts',(0.205276678568417,0.219605090033885,
1.72686655424502)) ;
#50125=CARTESIAN_POINT('Ctrl Pts',(0.22386989322167,0.201428663227279,1.70350036667433)) ;
#50126=CARTESIAN_POINT('Ctrl Pts',(0.256050927678194,0.158678076494978,
1.66597959949031)) ;
#50127=CARTESIAN_POINT('Ctrl Pts',(0.272049768241992,0.13073954601732,1.6494715036482)) ;
#50128=CARTESIAN_POINT('Ctrl Pts',(0.294064901325084,0.0680421958529071,
1.6272468646998)) ;
#50129=CARTESIAN_POINT('Ctrl Pts',(0.3,0.0332423590517548,1.62156571262682)) ;
#50130=CARTESIAN_POINT('Ctrl Pts',(0.3,-0.0332423590517547,1.62156571262682)) ;
#50131=CARTESIAN_POINT('Ctrl Pts',(0.294064901325084,-0.068042195852907,
1.6272468646998)) ;
#50132=CARTESIAN_POINT('Ctrl Pts',(0.272049768241992,-0.13073954601732,
1.6494715036482)) ;
#50133=CARTESIAN_POINT('Ctrl Pts',(0.256050927678194,-0.158678076494978,
1.66597959949031)) ;
#50134=CARTESIAN_POINT('Ctrl Pts',(0.22386989322167,-0.201428663227279,
1.70350036667433)) ;
#50135=CARTESIAN_POINT('Ctrl Pts',(0.205276678568417,-0.219605090033885,
1.72686655424502)) ;
#50136=CARTESIAN_POINT('Ctrl Pts',(0.183141637145543,-0.237803273510375,
1.76748264287115)) ;
#50137=CARTESIAN_POINT('Ctrl Pts',(0.176787603683127,-0.242434088321297,
1.782012704586)) ;
#50138=CARTESIAN_POINT('Ctrl Pts',(0.172184099341621,-0.24566794421234,
1.79815279520613)) ;
#50139=CARTESIAN_POINT('Ctrl Pts',(0.171928929654082,-0.245846566893906,
1.799075207463)) ;
#50140=CARTESIAN_POINT('Ctrl Pts',(0.171681132240627,-0.246019488725134,
1.8)) ;
#50141=CARTESIAN_POINT('',(1.64540693022728E-16,0.25,1.8)) ;
#50142=CARTESIAN_POINT('Origin',(5.27355936696949E-16,0.,1.8)) ;
#50143=CARTESIAN_POINT('',(5.55111512312578E-17,3.06161699786839E-17,2.05881904510252)) ;
#50144=CARTESIAN_POINT('Origin',(0.,0.,1.8)) ;
#50145=CARTESIAN_POINT('',(0.370590477448738,3.06161699786838E-17,2.15811846425757)) ;
#50146=CARTESIAN_POINT('',(0.18529523872437,3.06161699786838E-17,2.10846875468005)) ;
#50147=CARTESIAN_POINT('',(0.5,0.25,1.93397459621556)) ;
#50148=CARTESIAN_POINT('Origin',(0.499999999999999,0.,1.93397459621556)) ;
#50149=CARTESIAN_POINT('',(0.5,-0.25,1.93397459621556)) ;
#50150=CARTESIAN_POINT('Origin',(0.5,0.,1.93397459621556)) ;
#50151=CARTESIAN_POINT('Origin',(0.499999999999999,0.,1.93397459621556)) ;
#50152=CARTESIAN_POINT('Origin',(0.,0.,1.8)) ;
#50153=CARTESIAN_POINT('Origin',(1.,0.,2.8)) ;
#50154=CARTESIAN_POINT('',(1.,0.25,2.8)) ;
#50155=CARTESIAN_POINT('',(1.,-0.25,2.8)) ;
#50156=CARTESIAN_POINT('Origin',(1.,0.,2.8)) ;
#50157=CARTESIAN_POINT('Origin',(1.,0.,2.8)) ;
#50158=CARTESIAN_POINT('Origin',(0.866025403784438,0.,3.3)) ;
#50159=CARTESIAN_POINT('',(0.866025403784438,-0.25,3.3)) ;
#50160=CARTESIAN_POINT('',(0.866025403784438,0.25,3.3)) ;
#50161=CARTESIAN_POINT('Origin',(0.866025403784438,0.,3.3)) ;
#50162=CARTESIAN_POINT('Origin',(0.866025403784438,0.,3.3)) ;
#50163=CARTESIAN_POINT('Origin',(0.5,0.,3.66602540378444)) ;
#50164=CARTESIAN_POINT('',(0.499999999999999,-0.25,3.66602540378444)) ;
#50165=CARTESIAN_POINT('',(0.499999999999999,0.25,3.66602540378444)) ;
#50166=CARTESIAN_POINT('Origin',(0.5,0.,3.66602540378444)) ;
#50167=CARTESIAN_POINT('Origin',(0.5,0.,3.66602540378444)) ;
#50168=CARTESIAN_POINT('Origin',(-1.83697019872103E-16,0.,3.8)) ;
#50169=CARTESIAN_POINT('',(-1.12986998865286E-18,-0.25,3.8)) ;
#50170=CARTESIAN_POINT('',(-1.12986998865286E-18,0.25,3.8)) ;
#50171=CARTESIAN_POINT('Origin',(-1.94289029309402E-16,0.,3.8)) ;
#50172=CARTESIAN_POINT('',(-0.0647047612756307,-7.92404787857945E-18,4.04148145657227)) ;
#50173=CARTESIAN_POINT('Origin',(-2.22044604925031E-16,0.,3.8)) ;
#50174=CARTESIAN_POINT('',(-1.99005104861445E-16,-1.87469972832732E-33,
4.05)) ;
#50175=CARTESIAN_POINT('Origin',(-1.83697019872103E-16,0.,3.8)) ;
#50176=CARTESIAN_POINT('Origin',(-2.22044604925031E-16,0.,3.8)) ;
#50177=CARTESIAN_POINT('Origin',(-0.5,0.,3.66602540378444)) ;
#50178=CARTESIAN_POINT('',(-0.5,-0.25,3.66602540378444)) ;
#50179=CARTESIAN_POINT('',(-0.564704761275631,-3.06161699786838E-17,3.90750686035671)) ;
#50180=CARTESIAN_POINT('Origin',(-0.5,0.,3.66602540378444)) ;
#50181=CARTESIAN_POINT('',(-0.5,0.25,3.66602540378444)) ;
#50182=CARTESIAN_POINT('Origin',(-0.5,0.,3.66602540378444)) ;
#50183=CARTESIAN_POINT('',(-0.676776695296637,-3.06161699786838E-17,3.84280209908108)) ;
#50184=CARTESIAN_POINT('Origin',(-0.5,0.,3.66602540378444)) ;
#50185=CARTESIAN_POINT('Origin',(-0.5,0.,3.66602540378444)) ;
#50186=CARTESIAN_POINT('Origin',(-0.866025403784439,0.,3.3)) ;
#50187=CARTESIAN_POINT('',(-0.866025403784439,-0.25,3.3)) ;
#50188=CARTESIAN_POINT('',(-1.04280209908108,-3.06161699786838E-17,3.47677669529664)) ;
#50189=CARTESIAN_POINT('Origin',(-0.866025403784439,0.,3.3)) ;
#50190=CARTESIAN_POINT('',(-0.866025403784439,0.25,3.3)) ;
#50191=CARTESIAN_POINT('Origin',(-0.866025403784439,0.,3.3)) ;
#50192=CARTESIAN_POINT('',(-1.10750686035671,-3.06161699786838E-17,3.36470476127563)) ;
#50193=CARTESIAN_POINT('Origin',(-0.866025403784439,0.,3.3)) ;
#50194=CARTESIAN_POINT('Origin',(-0.866025403784439,0.,3.3)) ;
#50195=CARTESIAN_POINT('Origin',(-1.,0.,2.8)) ;
#50196=CARTESIAN_POINT('',(-1.,-0.25,2.8)) ;
#50197=CARTESIAN_POINT('',(-1.24148145657227,-3.06161699786838E-17,2.86470476127563)) ;
#50198=CARTESIAN_POINT('Origin',(-1.,0.,2.8)) ;
#50199=CARTESIAN_POINT('',(-1.,0.25,2.8)) ;
#50200=CARTESIAN_POINT('Origin',(-1.,0.,2.8)) ;
#50201=CARTESIAN_POINT('',(-1.24148145657227,-3.06161699786838E-17,2.73529523872437)) ;
#50202=CARTESIAN_POINT('Origin',(-1.,0.,2.8)) ;
#50203=CARTESIAN_POINT('Origin',(-1.,0.,2.8)) ;
#50204=CARTESIAN_POINT('Origin',(-0.866025403784439,0.,2.3)) ;
#50205=CARTESIAN_POINT('',(-0.866025403784439,-0.25,2.3)) ;
#50206=CARTESIAN_POINT('',(-1.10750686035671,-3.06161699786838E-17,2.23529523872437)) ;
#50207=CARTESIAN_POINT('Origin',(-0.866025403784439,0.,2.3)) ;
#50208=CARTESIAN_POINT('',(-0.866025403784439,0.25,2.3)) ;
#50209=CARTESIAN_POINT('Origin',(-0.866025403784439,0.,2.3)) ;
#50210=CARTESIAN_POINT('',(-1.04280209908108,-3.06161699786838E-17,2.12322330470336)) ;
#50211=CARTESIAN_POINT('Origin',(-0.866025403784439,0.,2.3)) ;
#50212=CARTESIAN_POINT('Origin',(-0.866025403784439,0.,2.3)) ;
#50213=CARTESIAN_POINT('Origin',(-0.5,0.,1.93397459621556)) ;
#50214=CARTESIAN_POINT('',(-0.5,-0.25,1.93397459621556)) ;
#50215=CARTESIAN_POINT('',(-0.676776695296637,-3.06161699786838E-17,1.75719790091892)) ;
#50216=CARTESIAN_POINT('Origin',(-0.5,0.,1.93397459621556)) ;
#50217=CARTESIAN_POINT('',(-0.5,0.25,1.93397459621556)) ;
#50218=CARTESIAN_POINT('Origin',(-0.5,0.,1.93397459621556)) ;
#50219=CARTESIAN_POINT('',(-0.56470476127563,-3.06161699786838E-17,1.69249313964329)) ;
#50220=CARTESIAN_POINT('Origin',(-0.5,0.,1.93397459621556)) ;
#50221=CARTESIAN_POINT('Origin',(-0.5,0.,1.93397459621556)) ;
#50222=CARTESIAN_POINT('Origin',(0.5,0.,1.93397459621556)) ;
#50223=CARTESIAN_POINT('Origin',(0.5,0.,1.93397459621556)) ;
#50224=CARTESIAN_POINT('Origin',(0.866025403784439,0.,2.3)) ;
#50225=CARTESIAN_POINT('',(0.866025403784438,-0.25,2.3)) ;
#50226=CARTESIAN_POINT('',(0.866025403784438,0.25,2.3)) ;
#50227=CARTESIAN_POINT('Origin',(0.866025403784439,0.,2.3)) ;
#50228=CARTESIAN_POINT('Origin',(0.866025403784439,0.,2.3)) ;
#50229=CARTESIAN_POINT('Origin',(0.933012701892219,0.,3.05)) ;
#50230=CARTESIAN_POINT('',(0.741180954897479,3.06161699786838E-17,2.8)) ;
#50231=CARTESIAN_POINT('Origin',(1.,0.,2.8)) ;
#50232=CARTESIAN_POINT('Origin',(1.,0.,2.8)) ;
#50233=CARTESIAN_POINT('',(0.641881535742425,3.06161699786838E-17,3.17059047744874)) ;
#50234=CARTESIAN_POINT('',(0.691531245319952,3.06161699786838E-17,2.98529523872437)) ;
#50235=CARTESIAN_POINT('Origin',(0.866025403784438,0.,3.3)) ;
#50236=CARTESIAN_POINT('Origin',(0.866025403784438,0.,3.3)) ;
#50237=CARTESIAN_POINT('Origin',(0.683012701892219,0.,3.48301270189222)) ;
#50238=CARTESIAN_POINT('',(0.370590477448739,3.06161699786838E-17,3.44188153574243)) ;
#50239=CARTESIAN_POINT('',(0.506236006595582,3.06161699786838E-17,3.30623600659558)) ;
#50240=CARTESIAN_POINT('Origin',(0.5,0.,3.66602540378444)) ;
#50241=CARTESIAN_POINT('Origin',(0.5,0.,3.66602540378444)) ;
#50242=CARTESIAN_POINT('Origin',(0.25,0.,3.73301270189222)) ;
#50243=CARTESIAN_POINT('',(-3.46944695195361E-16,3.06161699786838E-17,3.54118095489748)) ;
#50244=CARTESIAN_POINT('',(0.185295238724369,3.06161699786838E-17,3.49153124531995)) ;
#50245=CARTESIAN_POINT('Origin',(-2.4980018054066E-16,0.,3.8)) ;
#50246=CARTESIAN_POINT('Origin',(-2.4980018054066E-16,0.,3.8)) ;
#50247=CARTESIAN_POINT('Origin',(-0.25,0.,3.73301270189222)) ;
#50248=CARTESIAN_POINT('',(-0.314704761275631,-3.06161699786838E-17,3.97449415846449)) ;
#50249=CARTESIAN_POINT('Origin',(-0.5,0.,3.66602540378444)) ;
#50250=CARTESIAN_POINT('Origin',(-0.68301270189222,0.,3.48301270189222)) ;
#50251=CARTESIAN_POINT('',(-0.859789397188856,-3.06161699786838E-17,3.65978939718886)) ;
#50252=CARTESIAN_POINT('Origin',(-0.866025403784439,0.,3.3)) ;
#50253=CARTESIAN_POINT('Origin',(-0.933012701892219,0.,3.05)) ;
#50254=CARTESIAN_POINT('',(-1.17449415846449,-3.06161699786838E-17,3.11470476127563)) ;
#50255=CARTESIAN_POINT('Origin',(-1.,0.,2.8)) ;
#50256=CARTESIAN_POINT('Origin',(-0.933012701892219,0.,2.55)) ;
#50257=CARTESIAN_POINT('',(-1.17449415846449,-3.06161699786838E-17,2.48529523872437)) ;
#50258=CARTESIAN_POINT('Origin',(-0.866025403784439,0.,2.3)) ;
#50259=CARTESIAN_POINT('Origin',(-0.683012701892219,0.,2.11698729810778)) ;
#50260=CARTESIAN_POINT('',(-0.859789397188856,-3.06161699786838E-17,1.94021060281114)) ;
#50261=CARTESIAN_POINT('Origin',(-0.5,0.,1.93397459621556)) ;
#50262=CARTESIAN_POINT('Origin',(-0.25,0.,1.86698729810778)) ;
#50263=CARTESIAN_POINT('',(-0.3,5.50859672237977E-18,1.62156571262682)) ;
#50264=CARTESIAN_POINT('',(-0.31470476127563,-3.06161699786838E-17,1.62550584153551)) ;
#50265=CARTESIAN_POINT('',(-0.171681132240627,-0.246019488725134,1.8)) ;
#50266=CARTESIAN_POINT('Ctrl Pts',(-0.171681132240627,-0.246019488725134,
1.8)) ;
#50267=CARTESIAN_POINT('Ctrl Pts',(-0.172207810962449,-0.245651953617416,
1.79803440825089)) ;
#50268=CARTESIAN_POINT('Ctrl Pts',(-0.172767621079718,-0.245258790470191,
1.7960802634788)) ;
#50269=CARTESIAN_POINT('Ctrl Pts',(-0.178257858233088,-0.241371425647844,
1.77805114730154)) ;
#50270=CARTESIAN_POINT('Ctrl Pts',(-0.185355094601362,-0.236127799089863,
1.76280751800332)) ;
#50271=CARTESIAN_POINT('Ctrl Pts',(-0.209709816425776,-0.215576225066061,
1.72038403302066)) ;
#50272=CARTESIAN_POINT('Ctrl Pts',(-0.229722022348292,-0.195109377237531,
1.69623535556665)) ;
#50273=CARTESIAN_POINT('Ctrl Pts',(-0.26112090484938,-0.149973351529612,
1.66067985684946)) ;
#50274=CARTESIAN_POINT('Ctrl Pts',(-0.275367273146093,-0.123095023040758,
1.6460810308757)) ;
#50275=CARTESIAN_POINT('Ctrl Pts',(-0.294844938349426,-0.063608040301515,
1.62651059381835)) ;
#50276=CARTESIAN_POINT('Ctrl Pts',(-0.3,-0.0309656629660992,1.62156571262682)) ;
#50277=CARTESIAN_POINT('Ctrl Pts',(-0.3,3.46944695195361E-17,1.62156571262682)) ;
#50278=CARTESIAN_POINT('Origin',(5.55111512312578E-17,0.,1.8)) ;
#50279=CARTESIAN_POINT('',(-0.171681132240627,0.246019488725134,1.8)) ;
#50280=CARTESIAN_POINT('Origin',(5.55111512312578E-17,0.,1.8)) ;
#50281=CARTESIAN_POINT('Ctrl Pts',(-0.3,2.77555756156289E-17,1.62156571262682)) ;
#50282=CARTESIAN_POINT('Ctrl Pts',(-0.3,0.0309656629660992,1.62156571262682)) ;
#50283=CARTESIAN_POINT('Ctrl Pts',(-0.294844938349426,0.0636080403015151,
1.62651059381835)) ;
#50284=CARTESIAN_POINT('Ctrl Pts',(-0.275367273146093,0.123095023040759,
1.6460810308757)) ;
#50285=CARTESIAN_POINT('Ctrl Pts',(-0.26112090484938,0.149973351529612,
1.66067985684946)) ;
#50286=CARTESIAN_POINT('Ctrl Pts',(-0.229722022348292,0.195109377237531,
1.69623535556665)) ;
#50287=CARTESIAN_POINT('Ctrl Pts',(-0.209709816425776,0.215576225066061,
1.72038403302066)) ;
#50288=CARTESIAN_POINT('Ctrl Pts',(-0.185355094601362,0.236127799089863,
1.76280751800332)) ;
#50289=CARTESIAN_POINT('Ctrl Pts',(-0.178257858233088,0.241371425647844,
1.77805114730154)) ;
#50290=CARTESIAN_POINT('Ctrl Pts',(-0.172767621079718,0.245258790470192,
1.7960802634788)) ;
#50291=CARTESIAN_POINT('Ctrl Pts',(-0.172207810962449,0.245651953617416,
1.79803440825089)) ;
#50292=CARTESIAN_POINT('Ctrl Pts',(-0.171681132240627,0.246019488725134,
1.8)) ;
#50293=CARTESIAN_POINT('Origin',(0.683012701892219,0.,2.11698729810778)) ;
#50294=CARTESIAN_POINT('',(0.641881535742426,3.06161699786838E-17,2.42940952255126)) ;
#50295=CARTESIAN_POINT('',(0.506236006595582,3.06161699786838E-17,2.29376399340442)) ;
#50296=CARTESIAN_POINT('Origin',(0.866025403784439,0.,2.3)) ;
#50297=CARTESIAN_POINT('Origin',(0.866025403784439,0.,2.3)) ;
#50298=CARTESIAN_POINT('Origin',(0.933012701892219,0.,2.55)) ;
#50299=CARTESIAN_POINT('',(0.691531245319952,3.06161699786838E-17,2.61470476127563)) ;
#50300=CARTESIAN_POINT('Origin',(0.,0.,1.8)) ;
#50301=CARTESIAN_POINT('Origin',(0.,0.,1.8)) ;
#50302=CARTESIAN_POINT('Origin',(0.,0.,0.)) ;
#50303=CARTESIAN_POINT('',(-0.3,-3.67394039744206E-17,-1.8)) ;
#50304=CARTESIAN_POINT('',(-0.3,-3.67394039744206E-17,0.)) ;
#50305=CARTESIAN_POINT('Origin',(0.,0.,-1.8)) ;
#50306=CARTESIAN_POINT('Origin',(0.,0.,1.8)) ;
#50307=CARTESIAN_POINT('Origin',(0.,0.,-1.8)) ;
#50308=CARTESIAN_POINT('Origin',(0.,0.,1.8)) ;
#50386=UNCERTAINTY_MEASURE_WITH_UNIT(LENGTH_MEASURE(0.001),#50441,
'DISTANCE_ACCURACY_VALUE',
'Maximum model space distance between geometric entities at asserted c
onnectivities') ;
#50387=UNCERTAINTY_MEASURE_WITH_UNIT(LENGTH_MEASURE(0.001),#50441,
'DISTANCE_ACCURACY_VALUE',
'Maximum model space distance between geometric entities at asserted c
onnectivities') ;
#50439=(
GEOMETRIC_REPRESENTATION_CONTEXT(3)
GLOBAL_UNCERTAINTY_ASSIGNED_CONTEXT((#50386))
GLOBAL_UNIT_ASSIGNED_CONTEXT((#50441,#50443,#50444))
REPRESENTATION_CONTEXT('','3D')
) ;
#50440=(
GEOMETRIC_REPRESENTATION_CONTEXT(3)
GLOBAL_UNCERTAINTY_ASSIGNED_CONTEXT((#50387))
GLOBAL_UNIT_ASSIGNED_CONTEXT((#50441,#50443,#50444))
REPRESENTATION_CONTEXT('','3D')
) ;
#50441=(
LENGTH_UNIT()
NAMED_UNIT(*)
SI_UNIT(.CENTI.,.METRE.)
) ;
#50443=(
NAMED_UNIT(*)
PLANE_ANGLE_UNIT()
SI_UNIT($,.RADIAN.)
) ;
#50444=(
NAMED_UNIT(*)
SI_UNIT($,.STERADIAN.)
SOLID_ANGLE_UNIT()
) ;
#50496=SHAPE_DEFINITION_REPRESENTATION(#50592,#50670) ;
#50592=PRODUCT_DEFINITION_SHAPE('',$,#50723) ;
#50670=SHAPE_REPRESENTATION('',(#32277),#50439) ;
#50671=PRODUCT_DEFINITION_CONTEXT('part definition',#50829,'design') ;
#50723=PRODUCT_DEFINITION('LINCH_PIN','LINCH_PIN',#50775,
#50671) ;
#50775=PRODUCT_DEFINITION_FORMATION('',$,#50882) ;
#50829=APPLICATION_CONTEXT(
'Core Data for Automotive Mechanical Design Process') ;
#50830=PRODUCT_CONTEXT('part definition',#50829,'mechanical') ;
#50882=PRODUCT('LINCH_PIN','LINCH_PIN',$,(#50830)) ;
#50883=PRESENTATION_STYLE_ASSIGNMENT((#50890)) ;
#50890=SURFACE_STYLE_USAGE(.BOTH.,#50897) ;
#50897=SURFACE_SIDE_STYLE('',(#50904)) ;
#50904=SURFACE_STYLE_FILL_AREA(#50911) ;
#50911=FILL_AREA_STYLE('Steel - Satin',(#50918)) ;
#50918=FILL_AREA_STYLE_COLOUR('Steel - Satin',#50925) ;
#50925=COLOUR_RGB('Steel - Satin', 0.31764706, 0.68627451, 0.89019608) ;
ENDSEC;
END-ISO-10303-21;
